ISO-10303-21;
HEADER;
/* Generated by software containing ST-Developer
 * from STEP Tools, Inc. (www.steptools.com) 
 */

FILE_DESCRIPTION(
/* description */ (''),
/* implementation_level */ '2;1');

FILE_NAME(
/* name */ 'Pin_01.step',
/* time_stamp */ '2026-10-23T17:00:58+06:00',
/* author */ (''),
/* organization */ (''),
/* preprocessor_version */ 'ST-DEVELOPER v20.2',
/* originating_system */ 'Autodesk Translation Framework v15.15.0.0',
/* authorisation */ '');

FILE_SCHEMA (('AUTOMOTIVE_DESIGN { 1 0 10303 214 3 1 1 }'));
ENDSEC;

DATA;
#10=MECHANICAL_DESIGN_GEOMETRIC_PRESENTATION_REPRESENTATION('',(#107),#11385);
#81=SHAPE_REPRESENTATION_RELATIONSHIP('SRR','None',#11433,#94);
#94=ADVANCED_BREP_SHAPE_REPRESENTATION('',(#120),#11373);
#107=STYLED_ITEM('',(#11567),#120);
#120=MANIFOLD_SOLID_BREP('Pin_01',#5343);
#224=CONICAL_SURFACE('',#5780,0.7,0.785398163397451);
#225=CONICAL_SURFACE('',#5786,0.7,0.785398163397448);
#398=CIRCLE('',#5781,0.649999999999999);
#399=CIRCLE('',#5782,0.75);
#400=CIRCLE('',#5784,0.75);
#401=CIRCLE('',#5787,0.649999999999999);
#577=CYLINDRICAL_SURFACE('',#5783,0.75);
#757=FACE_OUTER_BOUND('',#1101,.T.);
#758=FACE_OUTER_BOUND('',#1102,.T.);
#759=FACE_OUTER_BOUND('',#1103,.T.);
#760=FACE_OUTER_BOUND('',#1104,.T.);
#761=FACE_OUTER_BOUND('',#1105,.T.);
#1101=EDGE_LOOP('',(#4134,#4135,#4136,#4137));
#1102=EDGE_LOOP('',(#4138,#4139,#4140,#4141));
#1103=EDGE_LOOP('',(#4142));
#1104=EDGE_LOOP('',(#4143,#4144,#4145,#4146));
#1105=EDGE_LOOP('',(#4147));
#1538=LINE('',#8561,#2000);
#1539=LINE('',#8565,#2001);
#1540=LINE('',#8570,#2002);
#2000=VECTOR('',#6917,0.7);
#2001=VECTOR('',#6922,0.75);
#2002=VECTOR('',#6929,0.7);
#2442=VERTEX_POINT('',#8558);
#2443=VERTEX_POINT('',#8560);
#2444=VERTEX_POINT('',#8564);
#2445=VERTEX_POINT('',#8569);
#3032=EDGE_CURVE('',#2442,#2442,#398,.T.);
#3033=EDGE_CURVE('',#2442,#2443,#1538,.T.);
#3034=EDGE_CURVE('',#2443,#2443,#399,.T.);
#3035=EDGE_CURVE('',#2443,#2444,#1539,.T.);
#3036=EDGE_CURVE('',#2444,#2444,#400,.T.);
#3037=EDGE_CURVE('',#2444,#2445,#1540,.T.);
#3038=EDGE_CURVE('',#2445,#2445,#401,.T.);
#4134=ORIENTED_EDGE('',*,*,#3032,.T.);
#4135=ORIENTED_EDGE('',*,*,#3033,.T.);
#4136=ORIENTED_EDGE('',*,*,#3034,.T.);
#4137=ORIENTED_EDGE('',*,*,#3033,.F.);
#4138=ORIENTED_EDGE('',*,*,#3034,.F.);
#4139=ORIENTED_EDGE('',*,*,#3035,.T.);
#4140=ORIENTED_EDGE('',*,*,#3036,.F.);
#4141=ORIENTED_EDGE('',*,*,#3035,.F.);
#4142=ORIENTED_EDGE('',*,*,#3032,.F.);
#4143=ORIENTED_EDGE('',*,*,#3036,.T.);
#4144=ORIENTED_EDGE('',*,*,#3037,.T.);
#4145=ORIENTED_EDGE('',*,*,#3038,.T.);
#4146=ORIENTED_EDGE('',*,*,#3037,.F.);
#4147=ORIENTED_EDGE('',*,*,#3038,.F.);
#4936=PLANE('',#5785);
#4937=PLANE('',#5788);
#5169=ADVANCED_FACE('',(#757),#224,.T.);
#5170=ADVANCED_FACE('',(#758),#577,.T.);
#5171=ADVANCED_FACE('',(#759),#4936,.T.);
#5172=ADVANCED_FACE('',(#760),#225,.T.);
#5173=ADVANCED_FACE('',(#761),#4937,.F.);
#5343=CLOSED_SHELL('',(#5169,#5170,#5171,#5172,#5173));
#5779=AXIS2_PLACEMENT_3D('',#8556,#6911,#6912);
#5780=AXIS2_PLACEMENT_3D('',#8557,#6913,#6914);
#5781=AXIS2_PLACEMENT_3D('',#8559,#6915,#6916);
#5782=AXIS2_PLACEMENT_3D('',#8562,#6918,#6919);
#5783=AXIS2_PLACEMENT_3D('',#8563,#6920,#6921);
#5784=AXIS2_PLACEMENT_3D('',#8566,#6923,#6924);
#5785=AXIS2_PLACEMENT_3D('',#8567,#6925,#6926);
#5786=AXIS2_PLACEMENT_3D('',#8568,#6927,#6928);
#5787=AXIS2_PLACEMENT_3D('',#8571,#6930,#6931);
#5788=AXIS2_PLACEMENT_3D('',#8572,#6932,#6933);
#6911=DIRECTION('axis',(0.,0.,1.));
#6912=DIRECTION('refdir',(1.,0.,0.));
#6913=DIRECTION('center_axis',(-1.,0.,0.));
#6914=DIRECTION('ref_axis',(0.,-1.,-1.22464679914735E-16));
#6915=DIRECTION('center_axis',(-1.,0.,0.));
#6916=DIRECTION('ref_axis',(0.,-1.,-1.22464679914735E-16));
#6917=DIRECTION('',(-0.707106781186545,0.707106781186549,1.73191211247099E-16));
#6918=DIRECTION('center_axis',(1.,0.,0.));
#6919=DIRECTION('ref_axis',(0.,-1.,-1.22464679914735E-16));
#6920=DIRECTION('center_axis',(1.,0.,0.));
#6921=DIRECTION('ref_axis',(0.,-1.,-1.22464679914735E-16));
#6922=DIRECTION('',(-1.,0.,0.));
#6923=DIRECTION('center_axis',(-1.,0.,0.));
#6924=DIRECTION('ref_axis',(0.,-1.,-1.22464679914735E-16));
#6925=DIRECTION('center_axis',(1.,0.,0.));
#6926=DIRECTION('ref_axis',(0.,-1.22464679914735E-16,1.));
#6927=DIRECTION('center_axis',(1.,0.,0.));
#6928=DIRECTION('ref_axis',(0.,-1.,-1.22464679914735E-16));
#6929=DIRECTION('',(-0.707106781186548,-0.707106781186548,-1.73191211247099E-16));
#6930=DIRECTION('center_axis',(1.,0.,0.));
#6931=DIRECTION('ref_axis',(0.,-1.,-1.22464679914735E-16));
#6932=DIRECTION('center_axis',(1.,0.,0.));
#6933=DIRECTION('ref_axis',(0.,-1.22464679914735E-16,1.));
#8556=CARTESIAN_POINT('',(0.,0.,0.));
#8557=CARTESIAN_POINT('Origin',(-2.24952178519528,11.2640879581285,17.6));
#8558=CARTESIAN_POINT('',(-2.19952178519528,11.9140879581285,17.6));
#8559=CARTESIAN_POINT('Origin',(-2.19952178519528,11.2640879581285,17.6));
#8560=CARTESIAN_POINT('',(-2.29952178519528,12.0140879581285,17.6));
#8561=CARTESIAN_POINT('',(-2.24952178519528,11.9640879581285,17.6));
#8562=CARTESIAN_POINT('Origin',(-2.29952178519528,11.2640879581285,17.6));
#8563=CARTESIAN_POINT('Origin',(-7.59952178519528,11.2640879581285,17.6));
#8564=CARTESIAN_POINT('',(-7.49952178519528,12.0140879581285,17.6));
#8565=CARTESIAN_POINT('',(-7.59952178519528,12.0140879581285,17.6));
#8566=CARTESIAN_POINT('Origin',(-7.49952178519528,11.2640879581285,17.6));
#8567=CARTESIAN_POINT('Origin',(-2.19952178519528,11.2640879581285,17.6));
#8568=CARTESIAN_POINT('Origin',(-7.54952178519528,11.2640879581285,17.6));
#8569=CARTESIAN_POINT('',(-7.59952178519528,11.9140879581285,17.6));
#8570=CARTESIAN_POINT('',(-7.54952178519528,11.9640879581285,17.6));
#8571=CARTESIAN_POINT('Origin',(-7.59952178519528,11.2640879581285,17.6));
#8572=CARTESIAN_POINT('Origin',(-7.59952178519528,11.2640879581285,17.6));
#11358=UNCERTAINTY_MEASURE_WITH_UNIT(LENGTH_MEASURE(0.01),#11386,
'DISTANCE_ACCURACY_VALUE',
'Maximum model space distance between geometric entities at asserted c
onnectivities');
#11370=UNCERTAINTY_MEASURE_WITH_UNIT(LENGTH_MEASURE(0.01),#11386,
'DISTANCE_ACCURACY_VALUE',
'Maximum model space distance between geometric entities at asserted c
onnectivities');
#11373=(
GEOMETRIC_REPRESENTATION_CONTEXT(3)
GLOBAL_UNCERTAINTY_ASSIGNED_CONTEXT((#11358))
GLOBAL_UNIT_ASSIGNED_CONTEXT((#11386,#11388,#11389))
REPRESENTATION_CONTEXT('','3D')
);
#11385=(
GEOMETRIC_REPRESENTATION_CONTEXT(3)
GLOBAL_UNCERTAINTY_ASSIGNED_CONTEXT((#11370))
GLOBAL_UNIT_ASSIGNED_CONTEXT((#11386,#11388,#11389))
REPRESENTATION_CONTEXT('','3D')
);
#11386=(
LENGTH_UNIT()
NAMED_UNIT(*)
SI_UNIT(.MILLI.,.METRE.)
);
#11388=(
NAMED_UNIT(*)
PLANE_ANGLE_UNIT()
SI_UNIT($,.RADIAN.)
);
#11389=(
NAMED_UNIT(*)
SI_UNIT($,.STERADIAN.)
SOLID_ANGLE_UNIT()
);
#11392=SHAPE_DEFINITION_REPRESENTATION(#11406,#11433);
#11406=PRODUCT_DEFINITION_SHAPE('',$,#11448);
#11433=SHAPE_REPRESENTATION('',(#5779),#11373);
#11445=PRODUCT_DEFINITION_CONTEXT('part definition',#11489,'design');
#11448=PRODUCT_DEFINITION('Pin_01','Pin_01',#11462,#11445);
#11462=PRODUCT_DEFINITION_FORMATION('',$,#11493);
#11489=APPLICATION_CONTEXT(
'Core Data for Automotive Mechanical Design Process');
#11490=PRODUCT_CONTEXT('part definition',#11489,'mechanical');
#11493=PRODUCT('Pin_01','Pin_01',$,(#11490));
#11561=COLOUR_RGB('Grey',0.48,0.52,0.57);
#11562=FILL_AREA_STYLE_COLOUR('',#11561);
#11563=FILL_AREA_STYLE('',(#11562));
#11564=SURFACE_STYLE_FILL_AREA(#11563);
#11565=SURFACE_SIDE_STYLE('',(#11564));
#11566=SURFACE_STYLE_USAGE(.BOTH.,#11565);
#11567=PRESENTATION_STYLE_ASSIGNMENT((#11566));
ENDSEC;
END-ISO-10303-21;
